ISO-10303-21;
HEADER;
/* Generated by software containing ST-Developer
 * from STEP Tools, Inc. (www.steptools.com) 
 */

FILE_DESCRIPTION(
/* description */ ('Timing belt drive module 2 mm Pitch Timing 20T-40T'),

/* implementation_level */ '2;1');

FILE_NAME(
/* name */ 'Output M3 set screw.step',
/* time_stamp */ '2026-10-28T03:25:12-07:00',
/* author */ (''),
/* organization */ (''),
/* preprocessor_version */ 'ST-DEVELOPER v20.2',
/* originating_system */ 'Autodesk Translation Framework v15.17.0.0',
/* authorisation */ '');

FILE_SCHEMA (('AUTOMOTIVE_DESIGN { 1 0 10303 214 3 1 1 }'));
ENDSEC;

DATA;
#10=MECHANICAL_DESIGN_GEOMETRIC_PRESENTATION_REPRESENTATION('',(#577),#17830);
#476=SHAPE_REPRESENTATION_RELATIONSHIP('SRR','None',#18050,#519);
#519=ADVANCED_BREP_SHAPE_REPRESENTATION('',(#633),#17825);
#577=STYLED_ITEM('',(#18324),#633);
#633=MANIFOLD_SOLID_BREP('Body1',#9036);
#940=PLANE('',#10441);
#941=PLANE('',#10442);
#1363=FACE_OUTER_BOUND('',#2006,.T.);
#1364=FACE_OUTER_BOUND('',#2007,.T.);
#1365=FACE_OUTER_BOUND('',#2008,.T.);
#2006=EDGE_LOOP('',(#7533,#7534,#7535,#7536));
#2007=EDGE_LOOP('',(#7537));
#2008=EDGE_LOOP('',(#7538));
#2606=CIRCLE('',#10439,0.15);
#2607=CIRCLE('',#10440,0.15);
#3150=LINE('',#16728,#3628);
#3628=VECTOR('',#13017,0.15);
#4351=VERTEX_POINT('',#16725);
#4352=VERTEX_POINT('',#16727);
#5449=EDGE_CURVE('',#4351,#4351,#2606,.T.);
#5450=EDGE_CURVE('',#4351,#4352,#3150,.T.);
#5451=EDGE_CURVE('',#4352,#4352,#2607,.T.);
#7533=ORIENTED_EDGE('',*,*,#5449,.F.);
#7534=ORIENTED_EDGE('',*,*,#5450,.T.);
#7535=ORIENTED_EDGE('',*,*,#5451,.T.);
#7536=ORIENTED_EDGE('',*,*,#5450,.F.);
#7537=ORIENTED_EDGE('',*,*,#5449,.T.);
#7538=ORIENTED_EDGE('',*,*,#5451,.F.);
#8366=CYLINDRICAL_SURFACE('',#10438,0.15);
#8861=ADVANCED_FACE('',(#1363),#8366,.T.);
#8862=ADVANCED_FACE('',(#1364),#940,.T.);
#8863=ADVANCED_FACE('',(#1365),#941,.F.);
#9036=CLOSED_SHELL('',(#8861,#8862,#8863));
#10437=AXIS2_PLACEMENT_3D('',#16723,#13011,#13012);
#10438=AXIS2_PLACEMENT_3D('',#16724,#13013,#13014);
#10439=AXIS2_PLACEMENT_3D('',#16726,#13015,#13016);
#10440=AXIS2_PLACEMENT_3D('',#16729,#13018,#13019);
#10441=AXIS2_PLACEMENT_3D('',#16730,#13020,#13021);
#10442=AXIS2_PLACEMENT_3D('',#16731,#13022,#13023);
#13011=DIRECTION('axis',(0.,0.,1.));
#13012=DIRECTION('refdir',(1.,0.,0.));
#13013=DIRECTION('center_axis',(0.,0.,1.));
#13014=DIRECTION('ref_axis',(1.,0.,0.));
#13015=DIRECTION('center_axis',(0.,0.,1.));
#13016=DIRECTION('ref_axis',(1.,0.,0.));
#13017=DIRECTION('',(0.,0.,-1.));
#13018=DIRECTION('center_axis',(0.,0.,1.));
#13019=DIRECTION('ref_axis',(1.,0.,0.));
#13020=DIRECTION('center_axis',(0.,0.,1.));
#13021=DIRECTION('ref_axis',(1.,0.,0.));
#13022=DIRECTION('center_axis',(0.,0.,1.));
#13023=DIRECTION('ref_axis',(1.,0.,0.));
#16723=CARTESIAN_POINT('',(0.,0.,0.));
#16724=CARTESIAN_POINT('Origin',(6.97091003018116,-4.,6.));
#16725=CARTESIAN_POINT('',(6.82091003018116,-4.,6.4));
#16726=CARTESIAN_POINT('Origin',(6.97091003018116,-4.,6.4));
#16727=CARTESIAN_POINT('',(6.82091003018116,-4.,6.));
#16728=CARTESIAN_POINT('',(6.82091003018116,-4.,6.));
#16729=CARTESIAN_POINT('Origin',(6.97091003018116,-4.,6.));
#16730=CARTESIAN_POINT('Origin',(6.97091003018116,-4.,6.4));
#16731=CARTESIAN_POINT('Origin',(6.97091003018116,-4.,6.));
#17775=UNCERTAINTY_MEASURE_WITH_UNIT(LENGTH_MEASURE(0.001),#17831,
'DISTANCE_ACCURACY_VALUE',
'Maximum model space distance between geometric entities at asserted c
onnectivities');
#17780=UNCERTAINTY_MEASURE_WITH_UNIT(LENGTH_MEASURE(0.001),#17831,
'DISTANCE_ACCURACY_VALUE',
'Maximum model space distance between geometric entities at asserted c
onnectivities');
#17825=(
GEOMETRIC_REPRESENTATION_CONTEXT(3)
GLOBAL_UNCERTAINTY_ASSIGNED_CONTEXT((#17775))
GLOBAL_UNIT_ASSIGNED_CONTEXT((#17831,#17833,#17834))
REPRESENTATION_CONTEXT('','3D')
);
#17830=(
GEOMETRIC_REPRESENTATION_CONTEXT(3)
GLOBAL_UNCERTAINTY_ASSIGNED_CONTEXT((#17780))
GLOBAL_UNIT_ASSIGNED_CONTEXT((#17831,#17833,#17834))
REPRESENTATION_CONTEXT('','3D')
);
#17831=(
LENGTH_UNIT()
NAMED_UNIT(*)
SI_UNIT(.CENTI.,.METRE.)
);
#17833=(
NAMED_UNIT(*)
PLANE_ANGLE_UNIT()
SI_UNIT($,.RADIAN.)
);
#17834=(
NAMED_UNIT(*)
SI_UNIT($,.STERADIAN.)
SOLID_ANGLE_UNIT()
);
#17879=SHAPE_DEFINITION_REPRESENTATION(#17938,#18050);
#17938=PRODUCT_DEFINITION_SHAPE('',$,#18100);
#18050=SHAPE_REPRESENTATION('',(#10437),#17825);
#18055=PRODUCT_DEFINITION_CONTEXT('part definition',#18204,'design');
#18100=PRODUCT_DEFINITION('Output M3 set screw','Output M3 set screw',#18149,
#18055);
#18149=PRODUCT_DEFINITION_FORMATION('',$,#18250);
#18204=APPLICATION_CONTEXT(
'Core Data for Automotive Mechanical Design Process');
#18205=PRODUCT_CONTEXT('part definition',#18204,'mechanical');
#18250=PRODUCT('Output M3 set screw','Output M3 set screw',
'Output M3 set screw',(#18205));
#18318=COLOUR_RGB('Black',0.12,0.14,0.17);
#18319=FILL_AREA_STYLE_COLOUR('',#18318);
#18320=FILL_AREA_STYLE('',(#18319));
#18321=SURFACE_STYLE_FILL_AREA(#18320);
#18322=SURFACE_SIDE_STYLE('',(#18321));
#18323=SURFACE_STYLE_USAGE(.BOTH.,#18322);
#18324=PRESENTATION_STYLE_ASSIGNMENT((#18323));
ENDSEC;
END-ISO-10303-21;
